ISO-10303-21;
HEADER;
/* Generated by software containing ST-Developer
 * from STEP Tools, Inc. (www.steptools.com) 
 */

FILE_DESCRIPTION(
/* description */ ('PAT-082'),
/* implementation_level */ '2;1');

FILE_NAME(
/* name */ 'Outlet tube.step',
/* time_stamp */ '2026-10-29T20:16:13-07:00',
/* author */ (''),
/* organization */ (''),
/* preprocessor_version */ 'ST-DEVELOPER v20.2',
/* originating_system */ 'Autodesk Translation Framework v15.17.0.0',
/* authorisation */ '');

FILE_SCHEMA (('AUTOMOTIVE_DESIGN { 1 0 10303 214 3 1 1 }'));
ENDSEC;

DATA;
#10=MECHANICAL_DESIGN_GEOMETRIC_PRESENTATION_REPRESENTATION('',(#249),#8266);
#205=SHAPE_REPRESENTATION_RELATIONSHIP('SRR','None',#8367,#227);
#227=ADVANCED_BREP_SHAPE_REPRESENTATION('',(#271),#8251);
#249=STYLED_ITEM('',(#8530),#271);
#271=MANIFOLD_SOLID_BREP('Body1',#4589);
#376=FACE_BOUND('',#1082,.T.);
#377=FACE_BOUND('',#1084,.T.);
#487=PLANE('',#5136);
#488=PLANE('',#5137);
#715=FACE_OUTER_BOUND('',#1079,.T.);
#716=FACE_OUTER_BOUND('',#1080,.T.);
#717=FACE_OUTER_BOUND('',#1081,.T.);
#718=FACE_OUTER_BOUND('',#1083,.T.);
#1079=EDGE_LOOP('',(#3752,#3753,#3754,#3755));
#1080=EDGE_LOOP('',(#3756,#3757,#3758,#3759));
#1081=EDGE_LOOP('',(#3760));
#1082=EDGE_LOOP('',(#3761));
#1083=EDGE_LOOP('',(#3762));
#1084=EDGE_LOOP('',(#3763));
#1428=LINE('',#7655,#1783);
#1429=LINE('',#7661,#1784);
#1783=VECTOR('',#6141,0.2);
#1784=VECTOR('',#6148,0.3);
#2073=CIRCLE('',#5131,0.2);
#2074=CIRCLE('',#5132,0.2);
#2075=CIRCLE('',#5134,0.3);
#2076=CIRCLE('',#5135,0.3);
#2367=VERTEX_POINT('',#7652);
#2368=VERTEX_POINT('',#7654);
#2369=VERTEX_POINT('',#7658);
#2370=VERTEX_POINT('',#7660);
#2852=EDGE_CURVE('',#2367,#2367,#2073,.T.);
#2853=EDGE_CURVE('',#2367,#2368,#1428,.T.);
#2854=EDGE_CURVE('',#2368,#2368,#2074,.T.);
#2855=EDGE_CURVE('',#2369,#2369,#2075,.T.);
#2856=EDGE_CURVE('',#2369,#2370,#1429,.T.);
#2857=EDGE_CURVE('',#2370,#2370,#2076,.T.);
#3752=ORIENTED_EDGE('',*,*,#2852,.F.);
#3753=ORIENTED_EDGE('',*,*,#2853,.T.);
#3754=ORIENTED_EDGE('',*,*,#2854,.T.);
#3755=ORIENTED_EDGE('',*,*,#2853,.F.);
#3756=ORIENTED_EDGE('',*,*,#2855,.F.);
#3757=ORIENTED_EDGE('',*,*,#2856,.T.);
#3758=ORIENTED_EDGE('',*,*,#2857,.T.);
#3759=ORIENTED_EDGE('',*,*,#2856,.F.);
#3760=ORIENTED_EDGE('',*,*,#2855,.T.);
#3761=ORIENTED_EDGE('',*,*,#2852,.T.);
#3762=ORIENTED_EDGE('',*,*,#2857,.F.);
#3763=ORIENTED_EDGE('',*,*,#2854,.F.);
#4281=CYLINDRICAL_SURFACE('',#5130,0.2);
#4282=CYLINDRICAL_SURFACE('',#5133,0.3);
#4454=ADVANCED_FACE('',(#715),#4281,.F.);
#4455=ADVANCED_FACE('',(#716),#4282,.T.);
#4456=ADVANCED_FACE('',(#717,#376),#487,.T.);
#4457=ADVANCED_FACE('',(#718,#377),#488,.F.);
#4589=CLOSED_SHELL('',(#4454,#4455,#4456,#4457));
#5129=AXIS2_PLACEMENT_3D('',#7650,#6135,#6136);
#5130=AXIS2_PLACEMENT_3D('',#7651,#6137,#6138);
#5131=AXIS2_PLACEMENT_3D('',#7653,#6139,#6140);
#5132=AXIS2_PLACEMENT_3D('',#7656,#6142,#6143);
#5133=AXIS2_PLACEMENT_3D('',#7657,#6144,#6145);
#5134=AXIS2_PLACEMENT_3D('',#7659,#6146,#6147);
#5135=AXIS2_PLACEMENT_3D('',#7662,#6149,#6150);
#5136=AXIS2_PLACEMENT_3D('',#7663,#6151,#6152);
#5137=AXIS2_PLACEMENT_3D('',#7664,#6153,#6154);
#6135=DIRECTION('axis',(0.,0.,1.));
#6136=DIRECTION('refdir',(1.,0.,0.));
#6137=DIRECTION('center_axis',(0.,0.,1.));
#6138=DIRECTION('ref_axis',(1.,0.,0.));
#6139=DIRECTION('center_axis',(0.,0.,-1.));
#6140=DIRECTION('ref_axis',(1.,0.,0.));
#6141=DIRECTION('',(0.,0.,-1.));
#6142=DIRECTION('center_axis',(0.,0.,-1.));
#6143=DIRECTION('ref_axis',(1.,0.,0.));
#6144=DIRECTION('center_axis',(0.,0.,1.));
#6145=DIRECTION('ref_axis',(1.,0.,0.));
#6146=DIRECTION('center_axis',(0.,0.,1.));
#6147=DIRECTION('ref_axis',(1.,0.,0.));
#6148=DIRECTION('',(0.,0.,-1.));
#6149=DIRECTION('center_axis',(0.,0.,1.));
#6150=DIRECTION('ref_axis',(1.,0.,0.));
#6151=DIRECTION('center_axis',(0.,0.,1.));
#6152=DIRECTION('ref_axis',(1.,0.,0.));
#6153=DIRECTION('center_axis',(0.,0.,1.));
#6154=DIRECTION('ref_axis',(1.,0.,0.));
#7650=CARTESIAN_POINT('',(0.,0.,0.));
#7651=CARTESIAN_POINT('Origin',(-3.75,0.,5.7));
#7652=CARTESIAN_POINT('',(-3.95,-2.44929359829471E-17,8.95));
#7653=CARTESIAN_POINT('Origin',(-3.75,0.,8.95));
#7654=CARTESIAN_POINT('',(-3.95,-2.44929359829471E-17,5.7));
#7655=CARTESIAN_POINT('',(-3.95,-2.44929359829471E-17,5.7));
#7656=CARTESIAN_POINT('Origin',(-3.75,0.,5.7));
#7657=CARTESIAN_POINT('Origin',(-3.75,0.,5.7));
#7658=CARTESIAN_POINT('',(-4.05,-3.67394039744206E-17,8.95));
#7659=CARTESIAN_POINT('Origin',(-3.75,0.,8.95));
#7660=CARTESIAN_POINT('',(-4.05,-3.67394039744206E-17,5.7));
#7661=CARTESIAN_POINT('',(-4.05,-3.67394039744206E-17,5.7));
#7662=CARTESIAN_POINT('Origin',(-3.75,0.,5.7));
#7663=CARTESIAN_POINT('Origin',(-3.75,0.,8.95));
#7664=CARTESIAN_POINT('Origin',(-3.75,0.,5.7));
#8226=UNCERTAINTY_MEASURE_WITH_UNIT(LENGTH_MEASURE(0.001),#8267,
'DISTANCE_ACCURACY_VALUE',
'Maximum model space distance between geometric entities at asserted c
onnectivities');
#8241=UNCERTAINTY_MEASURE_WITH_UNIT(LENGTH_MEASURE(0.001),#8267,
'DISTANCE_ACCURACY_VALUE',
'Maximum model space distance between geometric entities at asserted c
onnectivities');
#8251=(
GEOMETRIC_REPRESENTATION_CONTEXT(3)
GLOBAL_UNCERTAINTY_ASSIGNED_CONTEXT((#8226))
GLOBAL_UNIT_ASSIGNED_CONTEXT((#8267,#8269,#8270))
REPRESENTATION_CONTEXT('','3D')
);
#8266=(
GEOMETRIC_REPRESENTATION_CONTEXT(3)
GLOBAL_UNCERTAINTY_ASSIGNED_CONTEXT((#8241))
GLOBAL_UNIT_ASSIGNED_CONTEXT((#8267,#8269,#8270))
REPRESENTATION_CONTEXT('','3D')
);
#8267=(
LENGTH_UNIT()
NAMED_UNIT(*)
SI_UNIT(.CENTI.,.METRE.)
);
#8269=(
NAMED_UNIT(*)
PLANE_ANGLE_UNIT()
SI_UNIT($,.RADIAN.)
);
#8270=(
NAMED_UNIT(*)
SI_UNIT($,.STERADIAN.)
SOLID_ANGLE_UNIT()
);
#8280=SHAPE_DEFINITION_REPRESENTATION(#8304,#8367);
#8304=PRODUCT_DEFINITION_SHAPE('',$,#8392);
#8367=SHAPE_REPRESENTATION('',(#5129),#8251);
#8382=PRODUCT_DEFINITION_CONTEXT('part definition',#8456,'design');
#8392=PRODUCT_DEFINITION('Outlet tube','Outlet tube',#8416,
#8382);
#8416=PRODUCT_DEFINITION_FORMATION('',$,#8467);
#8456=APPLICATION_CONTEXT(
'Core Data for Automotive Mechanical Design Process');
#8457=PRODUCT_CONTEXT('part definition',#8456,'mechanical');
#8467=PRODUCT('Outlet tube','Outlet tube','Outlet tube',(#8457));
#8524=COLOUR_RGB('Sky Blue',0.24,0.69,0.87);
#8525=FILL_AREA_STYLE_COLOUR('',#8524);
#8526=FILL_AREA_STYLE('',(#8525));
#8527=SURFACE_STYLE_FILL_AREA(#8526);
#8528=SURFACE_SIDE_STYLE('',(#8527));
#8529=SURFACE_STYLE_USAGE(.BOTH.,#8528);
#8530=PRESENTATION_STYLE_ASSIGNMENT((#8529));
ENDSEC;
END-ISO-10303-21;
